ISO-10303-21;
HEADER;
/* Generated by software containing ST-Developer
 * from STEP Tools, Inc. (www.steptools.com) 
 */

FILE_DESCRIPTION(
/* description */ ('Gravity roller conveyor section'),
/* implementation_level */ '2;1');

FILE_NAME(
/* name */ 'Cross foot (1).step',
/* time_stamp */ '2026-11-02T07:43:02-08:00',
/* author */ (''),
/* organization */ (''),
/* preprocessor_version */ 'ST-DEVELOPER v20.2',
/* originating_system */ 'Autodesk Translation Framework v15.17.0.0',
/* authorisation */ '');

FILE_SCHEMA (('AUTOMOTIVE_DESIGN { 1 0 10303 214 3 1 1 }'));
ENDSEC;

DATA;
#10=MECHANICAL_DESIGN_GEOMETRIC_PRESENTATION_REPRESENTATION('',(#540),#13821);
#472=SHAPE_REPRESENTATION_RELATIONSHIP('SRR','None',#14009,#506);
#506=ADVANCED_BREP_SHAPE_REPRESENTATION('',(#580),#13796);
#540=STYLED_ITEM('',(#14194),#580);
#580=MANIFOLD_SOLID_BREP('Body1',#7640);
#646=FACE_BOUND('',#1695,.T.);
#647=FACE_BOUND('',#1696,.T.);
#648=FACE_BOUND('',#1698,.T.);
#649=FACE_BOUND('',#1699,.T.);
#895=PLANE('',#8345);
#896=PLANE('',#8346);
#897=PLANE('',#8347);
#898=PLANE('',#8348);
#899=PLANE('',#8349);
#900=PLANE('',#8350);
#1232=FACE_OUTER_BOUND('',#1688,.T.);
#1233=FACE_OUTER_BOUND('',#1689,.T.);
#1234=FACE_OUTER_BOUND('',#1690,.T.);
#1235=FACE_OUTER_BOUND('',#1691,.T.);
#1236=FACE_OUTER_BOUND('',#1692,.T.);
#1237=FACE_OUTER_BOUND('',#1693,.T.);
#1238=FACE_OUTER_BOUND('',#1694,.T.);
#1239=FACE_OUTER_BOUND('',#1697,.T.);
#1688=EDGE_LOOP('',(#6378,#6379,#6380,#6381));
#1689=EDGE_LOOP('',(#6382,#6383,#6384,#6385));
#1690=EDGE_LOOP('',(#6386,#6387,#6388,#6389));
#1691=EDGE_LOOP('',(#6390,#6391,#6392,#6393));
#1692=EDGE_LOOP('',(#6394,#6395,#6396,#6397));
#1693=EDGE_LOOP('',(#6398,#6399,#6400,#6401));
#1694=EDGE_LOOP('',(#6402,#6403,#6404,#6405));
#1695=EDGE_LOOP('',(#6406));
#1696=EDGE_LOOP('',(#6407));
#1697=EDGE_LOOP('',(#6408,#6409,#6410,#6411));
#1698=EDGE_LOOP('',(#6412));
#1699=EDGE_LOOP('',(#6413));
#2464=LINE('',#12464,#3182);
#2465=LINE('',#12470,#3183);
#2466=LINE('',#12475,#3184);
#2467=LINE('',#12477,#3185);
#2468=LINE('',#12479,#3186);
#2469=LINE('',#12480,#3187);
#2470=LINE('',#12483,#3188);
#2471=LINE('',#12485,#3189);
#2472=LINE('',#12486,#3190);
#2473=LINE('',#12489,#3191);
#2474=LINE('',#12491,#3192);
#2475=LINE('',#12492,#3193);
#2476=LINE('',#12494,#3194);
#2477=LINE('',#12495,#3195);
#3182=VECTOR('',#9929,0.274999999999999);
#3183=VECTOR('',#9936,0.274999999999999);
#3184=VECTOR('',#9941,1.);
#3185=VECTOR('',#9942,1.);
#3186=VECTOR('',#9943,1.);
#3187=VECTOR('',#9944,1.);
#3188=VECTOR('',#9947,1.);
#3189=VECTOR('',#9948,1.);
#3190=VECTOR('',#9949,1.);
#3191=VECTOR('',#9952,1.);
#3192=VECTOR('',#9953,1.);
#3193=VECTOR('',#9954,1.);
#3194=VECTOR('',#9957,1.);
#3195=VECTOR('',#9958,1.);
#3426=CIRCLE('',#8340,0.274999999999999);
#3427=CIRCLE('',#8341,0.274999999999999);
#3428=CIRCLE('',#8343,0.274999999999999);
#3429=CIRCLE('',#8344,0.274999999999999);
#3980=VERTEX_POINT('',#12461);
#3981=VERTEX_POINT('',#12463);
#3982=VERTEX_POINT('',#12467);
#3983=VERTEX_POINT('',#12469);
#3984=VERTEX_POINT('',#12473);
#3985=VERTEX_POINT('',#12474);
#3986=VERTEX_POINT('',#12476);
#3987=VERTEX_POINT('',#12478);
#3988=VERTEX_POINT('',#12482);
#3989=VERTEX_POINT('',#12484);
#3990=VERTEX_POINT('',#12488);
#3991=VERTEX_POINT('',#12490);
#4826=EDGE_CURVE('',#3980,#3980,#3426,.T.);
#4827=EDGE_CURVE('',#3980,#3981,#2464,.T.);
#4828=EDGE_CURVE('',#3981,#3981,#3427,.T.);
#4829=EDGE_CURVE('',#3982,#3982,#3428,.T.);
#4830=EDGE_CURVE('',#3982,#3983,#2465,.T.);
#4831=EDGE_CURVE('',#3983,#3983,#3429,.T.);
#4832=EDGE_CURVE('',#3984,#3985,#2466,.T.);
#4833=EDGE_CURVE('',#3985,#3986,#2467,.T.);
#4834=EDGE_CURVE('',#3987,#3986,#2468,.T.);
#4835=EDGE_CURVE('',#3984,#3987,#2469,.T.);
#4836=EDGE_CURVE('',#3988,#3984,#2470,.T.);
#4837=EDGE_CURVE('',#3989,#3987,#2471,.T.);
#4838=EDGE_CURVE('',#3988,#3989,#2472,.T.);
#4839=EDGE_CURVE('',#3990,#3988,#2473,.T.);
#4840=EDGE_CURVE('',#3991,#3989,#2474,.T.);
#4841=EDGE_CURVE('',#3990,#3991,#2475,.T.);
#4842=EDGE_CURVE('',#3985,#3990,#2476,.T.);
#4843=EDGE_CURVE('',#3986,#3991,#2477,.T.);
#6378=ORIENTED_EDGE('',*,*,#4826,.F.);
#6379=ORIENTED_EDGE('',*,*,#4827,.T.);
#6380=ORIENTED_EDGE('',*,*,#4828,.F.);
#6381=ORIENTED_EDGE('',*,*,#4827,.F.);
#6382=ORIENTED_EDGE('',*,*,#4829,.F.);
#6383=ORIENTED_EDGE('',*,*,#4830,.T.);
#6384=ORIENTED_EDGE('',*,*,#4831,.F.);
#6385=ORIENTED_EDGE('',*,*,#4830,.F.);
#6386=ORIENTED_EDGE('',*,*,#4832,.T.);
#6387=ORIENTED_EDGE('',*,*,#4833,.T.);
#6388=ORIENTED_EDGE('',*,*,#4834,.F.);
#6389=ORIENTED_EDGE('',*,*,#4835,.F.);
#6390=ORIENTED_EDGE('',*,*,#4836,.T.);
#6391=ORIENTED_EDGE('',*,*,#4835,.T.);
#6392=ORIENTED_EDGE('',*,*,#4837,.F.);
#6393=ORIENTED_EDGE('',*,*,#4838,.F.);
#6394=ORIENTED_EDGE('',*,*,#4839,.T.);
#6395=ORIENTED_EDGE('',*,*,#4838,.T.);
#6396=ORIENTED_EDGE('',*,*,#4840,.F.);
#6397=ORIENTED_EDGE('',*,*,#4841,.F.);
#6398=ORIENTED_EDGE('',*,*,#4842,.T.);
#6399=ORIENTED_EDGE('',*,*,#4841,.T.);
#6400=ORIENTED_EDGE('',*,*,#4843,.F.);
#6401=ORIENTED_EDGE('',*,*,#4833,.F.);
#6402=ORIENTED_EDGE('',*,*,#4843,.T.);
#6403=ORIENTED_EDGE('',*,*,#4840,.T.);
#6404=ORIENTED_EDGE('',*,*,#4837,.T.);
#6405=ORIENTED_EDGE('',*,*,#4834,.T.);
#6406=ORIENTED_EDGE('',*,*,#4828,.T.);
#6407=ORIENTED_EDGE('',*,*,#4831,.T.);
#6408=ORIENTED_EDGE('',*,*,#4842,.F.);
#6409=ORIENTED_EDGE('',*,*,#4832,.F.);
#6410=ORIENTED_EDGE('',*,*,#4836,.F.);
#6411=ORIENTED_EDGE('',*,*,#4839,.F.);
#6412=ORIENTED_EDGE('',*,*,#4826,.T.);
#6413=ORIENTED_EDGE('',*,*,#4829,.T.);
#7154=CYLINDRICAL_SURFACE('',#8339,0.274999999999999);
#7155=CYLINDRICAL_SURFACE('',#8342,0.274999999999999);
#7433=ADVANCED_FACE('',(#1232),#7154,.F.);
#7434=ADVANCED_FACE('',(#1233),#7155,.F.);
#7435=ADVANCED_FACE('',(#1234),#895,.T.);
#7436=ADVANCED_FACE('',(#1235),#896,.T.);
#7437=ADVANCED_FACE('',(#1236),#897,.T.);
#7438=ADVANCED_FACE('',(#1237),#898,.T.);
#7439=ADVANCED_FACE('',(#1238,#646,#647),#899,.T.);
#7440=ADVANCED_FACE('',(#1239,#648,#649),#900,.F.);
#7640=CLOSED_SHELL('',(#7433,#7434,#7435,#7436,#7437,#7438,#7439,#7440));
#8338=AXIS2_PLACEMENT_3D('',#12459,#9923,#9924);
#8339=AXIS2_PLACEMENT_3D('',#12460,#9925,#9926);
#8340=AXIS2_PLACEMENT_3D('',#12462,#9927,#9928);
#8341=AXIS2_PLACEMENT_3D('',#12465,#9930,#9931);
#8342=AXIS2_PLACEMENT_3D('',#12466,#9932,#9933);
#8343=AXIS2_PLACEMENT_3D('',#12468,#9934,#9935);
#8344=AXIS2_PLACEMENT_3D('',#12471,#9937,#9938);
#8345=AXIS2_PLACEMENT_3D('',#12472,#9939,#9940);
#8346=AXIS2_PLACEMENT_3D('',#12481,#9945,#9946);
#8347=AXIS2_PLACEMENT_3D('',#12487,#9950,#9951);
#8348=AXIS2_PLACEMENT_3D('',#12493,#9955,#9956);
#8349=AXIS2_PLACEMENT_3D('',#12496,#9959,#9960);
#8350=AXIS2_PLACEMENT_3D('',#12497,#9961,#9962);
#9923=DIRECTION('axis',(0.,0.,1.));
#9924=DIRECTION('refdir',(1.,0.,0.));
#9925=DIRECTION('center_axis',(0.,0.,1.));
#9926=DIRECTION('ref_axis',(1.,0.,0.));
#9927=DIRECTION('center_axis',(0.,0.,1.));
#9928=DIRECTION('ref_axis',(1.,0.,0.));
#9929=DIRECTION('',(0.,0.,1.));
#9930=DIRECTION('center_axis',(0.,0.,-1.));
#9931=DIRECTION('ref_axis',(1.,0.,0.));
#9932=DIRECTION('center_axis',(0.,0.,1.));
#9933=DIRECTION('ref_axis',(1.,0.,0.));
#9934=DIRECTION('center_axis',(0.,0.,1.));
#9935=DIRECTION('ref_axis',(1.,0.,0.));
#9936=DIRECTION('',(0.,0.,1.));
#9937=DIRECTION('center_axis',(0.,0.,-1.));
#9938=DIRECTION('ref_axis',(1.,0.,0.));
#9939=DIRECTION('center_axis',(0.,1.,0.));
#9940=DIRECTION('ref_axis',(-1.,0.,0.));
#9941=DIRECTION('',(-1.,0.,0.));
#9942=DIRECTION('',(0.,0.,1.));
#9943=DIRECTION('',(-1.,0.,0.));
#9944=DIRECTION('',(0.,0.,1.));
#9945=DIRECTION('center_axis',(1.,0.,0.));
#9946=DIRECTION('ref_axis',(0.,1.,0.));
#9947=DIRECTION('',(0.,1.,0.));
#9948=DIRECTION('',(0.,1.,0.));
#9949=DIRECTION('',(0.,0.,1.));
#9950=DIRECTION('center_axis',(0.,-1.,0.));
#9951=DIRECTION('ref_axis',(1.,0.,0.));
#9952=DIRECTION('',(1.,0.,0.));
#9953=DIRECTION('',(1.,0.,0.));
#9954=DIRECTION('',(0.,0.,1.));
#9955=DIRECTION('center_axis',(-1.,0.,0.));
#9956=DIRECTION('ref_axis',(0.,-1.,0.));
#9957=DIRECTION('',(0.,-1.,0.));
#9958=DIRECTION('',(0.,-1.,0.));
#9959=DIRECTION('center_axis',(0.,0.,1.));
#9960=DIRECTION('ref_axis',(1.,0.,0.));
#9961=DIRECTION('center_axis',(0.,0.,1.));
#9962=DIRECTION('ref_axis',(1.,0.,0.));
#12459=CARTESIAN_POINT('',(0.,0.,0.));
#12460=CARTESIAN_POINT('Origin',(54.,-2.,-16.9));
#12461=CARTESIAN_POINT('',(53.725,-2.,-16.8));
#12462=CARTESIAN_POINT('Origin',(54.,-2.,-16.8));
#12463=CARTESIAN_POINT('',(53.725,-2.,-16.));
#12464=CARTESIAN_POINT('',(53.725,-2.,-16.9));
#12465=CARTESIAN_POINT('Origin',(54.,-2.,-16.));
#12466=CARTESIAN_POINT('Origin',(54.,32.,-16.9));
#12467=CARTESIAN_POINT('',(53.725,32.,-16.8));
#12468=CARTESIAN_POINT('Origin',(54.,32.,-16.8));
#12469=CARTESIAN_POINT('',(53.725,32.,-16.));
#12470=CARTESIAN_POINT('',(53.725,32.,-16.9));
#12471=CARTESIAN_POINT('Origin',(54.,32.,-16.));
#12472=CARTESIAN_POINT('Origin',(56.,35.,-16.8));
#12473=CARTESIAN_POINT('',(56.,35.,-16.8));
#12474=CARTESIAN_POINT('',(52.,35.,-16.8));
#12475=CARTESIAN_POINT('',(56.,35.,-16.8));
#12476=CARTESIAN_POINT('',(52.,35.,-16.));
#12477=CARTESIAN_POINT('',(52.,35.,-16.8));
#12478=CARTESIAN_POINT('',(56.,35.,-16.));
#12479=CARTESIAN_POINT('',(56.,35.,-16.));
#12480=CARTESIAN_POINT('',(56.,35.,-16.8));
#12481=CARTESIAN_POINT('Origin',(56.,-5.,-16.8));
#12482=CARTESIAN_POINT('',(56.,-5.,-16.8));
#12483=CARTESIAN_POINT('',(56.,-5.,-16.8));
#12484=CARTESIAN_POINT('',(56.,-5.,-16.));
#12485=CARTESIAN_POINT('',(56.,-5.,-16.));
#12486=CARTESIAN_POINT('',(56.,-5.,-16.8));
#12487=CARTESIAN_POINT('Origin',(52.,-5.,-16.8));
#12488=CARTESIAN_POINT('',(52.,-5.,-16.8));
#12489=CARTESIAN_POINT('',(52.,-5.,-16.8));
#12490=CARTESIAN_POINT('',(52.,-5.,-16.));
#12491=CARTESIAN_POINT('',(52.,-5.,-16.));
#12492=CARTESIAN_POINT('',(52.,-5.,-16.8));
#12493=CARTESIAN_POINT('Origin',(52.,35.,-16.8));
#12494=CARTESIAN_POINT('',(52.,35.,-16.8));
#12495=CARTESIAN_POINT('',(52.,35.,-16.));
#12496=CARTESIAN_POINT('Origin',(54.,15.,-16.));
#12497=CARTESIAN_POINT('Origin',(54.,15.,-16.8));
#13757=UNCERTAINTY_MEASURE_WITH_UNIT(LENGTH_MEASURE(0.001),#13822,
'DISTANCE_ACCURACY_VALUE',
'Maximum model space distance between geometric entities at asserted c
onnectivities');
#13782=UNCERTAINTY_MEASURE_WITH_UNIT(LENGTH_MEASURE(0.001),#13822,
'DISTANCE_ACCURACY_VALUE',
'Maximum model space distance between geometric entities at asserted c
onnectivities');
#13796=(
GEOMETRIC_REPRESENTATION_CONTEXT(3)
GLOBAL_UNCERTAINTY_ASSIGNED_CONTEXT((#13757))
GLOBAL_UNIT_ASSIGNED_CONTEXT((#13822,#13824,#13825))
REPRESENTATION_CONTEXT('','3D')
);
#13821=(
GEOMETRIC_REPRESENTATION_CONTEXT(3)
GLOBAL_UNCERTAINTY_ASSIGNED_CONTEXT((#13782))
GLOBAL_UNIT_ASSIGNED_CONTEXT((#13822,#13824,#13825))
REPRESENTATION_CONTEXT('','3D')
);
#13822=(
LENGTH_UNIT()
NAMED_UNIT(*)
SI_UNIT(.CENTI.,.METRE.)
);
#13824=(
NAMED_UNIT(*)
PLANE_ANGLE_UNIT()
SI_UNIT($,.RADIAN.)
);
#13825=(
NAMED_UNIT(*)
SI_UNIT($,.STERADIAN.)
SOLID_ANGLE_UNIT()
);
#13839=SHAPE_DEFINITION_REPRESENTATION(#13877,#14009);
#13877=PRODUCT_DEFINITION_SHAPE('',$,#14048);
#14009=SHAPE_REPRESENTATION('',(#8338),#13796);
#14034=PRODUCT_DEFINITION_CONTEXT('part definition',#14150,'design');
#14048=PRODUCT_DEFINITION('Cross foot_1','Cross foot (1)',#14086,#14034);
#14086=PRODUCT_DEFINITION_FORMATION('',$,#14165);
#14150=APPLICATION_CONTEXT(
'Core Data for Automotive Mechanical Design Process');
#14151=PRODUCT_CONTEXT('part definition',#14150,'mechanical');
#14165=PRODUCT('Cross foot_1','Cross foot (1)','Cross foot',(#14151));
#14194=PRESENTATION_STYLE_ASSIGNMENT((#14199));
#14199=SURFACE_STYLE_USAGE(.BOTH.,#14204);
#14204=SURFACE_SIDE_STYLE('',(#14209));
#14209=SURFACE_STYLE_FILL_AREA(#14214);
#14214=FILL_AREA_STYLE('CAD Library Painted - Deep blue',(#14219));
#14219=FILL_AREA_STYLE_COLOUR('CAD Library Painted - Deep blue',#14224);
#14224=COLOUR_RGB('CAD Library Painted - Deep blue',0.0784313725490196,
0.203921568627451,0.349019607843137);
ENDSEC;
END-ISO-10303-21;
